ISO-10303-21;
HEADER;
FILE_DESCRIPTION (('STEP AP214'),
    '1' );
FILE_NAME ('Base.step',
    '2026-10-23T20:35:44',
    ( '' ),
    ( '' ),
    'SwSTEP 2.0',
    'SolidWorks 2025',
    '' );
FILE_SCHEMA (( 'AUTOMOTIVE_DESIGN' ));
ENDSEC;

DATA;
#96=VERTEX_POINT ( 'NONE', #2710 ) ;
#103=VECTOR ( 'NONE', #1652, 39.37007874015748143 ) ;
#110=DIRECTION ( 'NONE',  ( -1.000000000000000000, 0.000000000000000000, 0.000000000000000000 ) ) ;
#111=CYLINDRICAL_SURFACE ( 'NONE', #3021, 0.2362204724409448231 ) ;
#113=CARTESIAN_POINT ( 'NONE',  ( -0.7480314960629922405, 1.220472440944881942, 0.000000000000000000 ) ) ;
#122=CIRCLE ( 'NONE', #5251, 1.968503937007874072 ) ;
#125=LINE ( 'NONE', #7263, #284 ) ;
#129=CARTESIAN_POINT ( 'NONE',  ( 2.834645669291338876, 0.4724409448818890911, 0.4724409448818898127 ) ) ;
#190=DIRECTION ( 'NONE',  ( -0.000000000000000000, -0.000000000000000000, -1.000000000000000000 ) ) ;
#203=DIRECTION ( 'NONE',  ( 0.000000000000000000, -0.000000000000000000, -1.000000000000000000 ) ) ;
#220=LINE ( 'NONE', #7202, #7073 ) ;
#234=ADVANCED_FACE ( 'NONE', ( #1554, #2883, #5130 ), #467, .T. ) ;
#253=ORIENTED_EDGE ( 'NONE', *, *, #5052, .T. ) ;
#255=ORIENTED_EDGE ( 'NONE', *, *, #2605, .T. ) ;
#256=EDGE_CURVE ( 'NONE', #3323, #5932, #1903, .T. ) ;
#263=CYLINDRICAL_SURFACE ( 'NONE', #3438, 0.2362204724409448231 ) ;
#268=DIRECTION ( 'NONE',  ( -1.000000000000000000, 0.000000000000000000, 0.000000000000000000 ) ) ;
#270=PRODUCT_DEFINITION_SHAPE ( 'NONE', 'NONE',  #6029 ) ;
#284=VECTOR ( 'NONE', #6774, 39.37007874015748143 ) ;
#294=CIRCLE ( 'NONE', #4189, 0.2362204724409448231 ) ;
#307=DIRECTION ( 'NONE',  ( -0.000000000000000000, -0.000000000000000000, -1.000000000000000000 ) ) ;
#321=VERTEX_POINT ( 'NONE', #3584 ) ;
#342=DIRECTION ( 'NONE',  ( -1.000000000000000000, 0.000000000000000000, -0.000000000000000000 ) ) ;
#344=CARTESIAN_POINT ( 'NONE',  ( -2.834645669291338432, 0.000000000000000000, 2.952755905511811108 ) ) ;
#350=PLANE ( 'NONE',  #1220 ) ;
#361=AXIS2_PLACEMENT_3D ( 'NONE', #4889, #1987, #872 ) ;
#369=CARTESIAN_POINT ( 'NONE',  ( -0.9842519685039370358, 1.220472440944881942, 0.000000000000000000 ) ) ;
#373=VECTOR ( 'NONE', #3196, 39.37007874015748143 ) ;
#379=CYLINDRICAL_SURFACE ( 'NONE', #5488, 1.968503937007874072 ) ;
#381=CARTESIAN_POINT ( 'NONE',  ( -1.279527559055117836, 1.968503937007873850, 2.952755905511811108 ) ) ;
#389=EDGE_CURVE ( 'NONE', #6862, #321, #1535, .T. ) ;
#418=CARTESIAN_POINT ( 'NONE',  ( 0.000000000000000000, 0.000000000000000000, 0.000000000000000000 ) ) ;
#428=VERTEX_POINT ( 'NONE', #369 ) ;
#447=LINE ( 'NONE', #1687, #103 ) ;
#454=CARTESIAN_POINT ( 'NONE',  ( 0.7480314960629922405, 1.220472440944881942, 0.4724409448818898127 ) ) ;
#462=LINE ( 'NONE', #2137, #1177 ) ;
#463=EDGE_LOOP ( 'NONE', ( #2691, #1742, #5296, #4406 ) ) ;
#467=PLANE ( 'NONE',  #1133 ) ;
#479=DIRECTION ( 'NONE',  ( 0.000000000000000000, 0.000000000000000000, -1.000000000000000000 ) ) ;
#489=VERTEX_POINT ( 'NONE', #3117 ) ;
#490=DIMENSIONAL_EXPONENTS ( 1.000000000000000000, 0.000000000000000000, 0.000000000000000000, 0.000000000000000000, 0.000000000000000000, 0.000000000000000000, 0.000000000000000000 ) ;
#492=PLANE ( 'NONE',  #7107 ) ;
#511=ORIENTED_EDGE ( 'NONE', *, *, #6690, .T. ) ;
#524=ORIENTED_EDGE ( 'NONE', *, *, #6050, .T. ) ;
#545=CARTESIAN_POINT ( 'NONE',  ( -2.834645669291338432, 0.4724409448818898127, 0.000000000000000000 ) ) ;
#552=DIRECTION ( 'NONE',  ( -1.000000000000000000, 0.000000000000000000, 0.000000000000000000 ) ) ;
#563=CARTESIAN_POINT ( 'NONE',  ( 0.5118110236220474452, 1.220472440944881942, 0.000000000000000000 ) ) ;
#612=ORIENTED_EDGE ( 'NONE', *, *, #4824, .F. ) ;
#629=EDGE_LOOP ( 'NONE', ( #6063, #5640 ) ) ;
#631=DIRECTION ( 'NONE',  ( -0.000000000000000000, -0.000000000000000000, 1.000000000000000000 ) ) ;
#638=CARTESIAN_POINT ( 'NONE',  ( 3.198568410424924124, 2.407012729153881203, 0.000000000000000000 ) ) ;
#643=DIRECTION ( 'NONE',  ( 0.000000000000000000, -0.000000000000000000, 1.000000000000000000 ) ) ;
#655=VERTEX_POINT ( 'NONE', #4638 ) ;
#656=PLANE ( 'NONE',  #1980 ) ;
#658=ORIENTED_EDGE ( 'NONE', *, *, #3656, .T. ) ;
#660=ADVANCED_FACE ( 'NONE', ( #2270 ), #492, .F. ) ;
#664=EDGE_CURVE ( 'NONE', #772, #6807, #4605, .T. ) ;
#670=VERTEX_POINT ( 'NONE', #6937 ) ;
#671=DIRECTION ( 'NONE',  ( -0.000000000000000000, -0.000000000000000000, -1.000000000000000000 ) ) ;
#673=APPLICATION_CONTEXT ( 'automotive_design' ) ;
#679=CARTESIAN_POINT ( 'NONE',  ( -2.834645669291338432, 0.000000000000000000, 0.000000000000000000 ) ) ;
#699=ORIENTED_EDGE ( 'NONE', *, *, #1392, .F. ) ;
#716=LINE ( 'NONE', #1979, #7122 ) ;
#729=LINE ( 'NONE', #768, #2227 ) ;
#749=LINE ( 'NONE', #5426, #4924 ) ;
#768=CARTESIAN_POINT ( 'NONE',  ( -2.834645669291338432, 0.000000000000000000, 0.4724409448818898127 ) ) ;
#772=VERTEX_POINT ( 'NONE', #129 ) ;
#775=ORIENTED_EDGE ( 'NONE', *, *, #256, .T. ) ;
#785=SHAPE_REPRESENTATION ( 'Base', ( #5166 ), #4425 ) ;
#786=ORIENTED_EDGE ( 'NONE', *, *, #5010, .F. ) ;
#792=DIRECTION ( 'NONE',  ( -0.000000000000000000, -0.000000000000000000, 1.000000000000000000 ) ) ;
#796=LINE ( 'NONE', #5434, #3412 ) ;
#800=EDGE_LOOP ( 'NONE', ( #7228, #4213, #2502, #2646 ) ) ;
#806=DIRECTION ( 'NONE',  ( -0.000000000000000000, -0.000000000000000000, -1.000000000000000000 ) ) ;
#809=EDGE_LOOP ( 'NONE', ( #524, #964, #2532, #4873 ) ) ;
#821=ORIENTED_EDGE ( 'NONE', *, *, #2617, .T. ) ;
#830=VECTOR ( 'NONE', #949, 39.37007874015748143 ) ;
#832=DIRECTION ( 'NONE',  ( -1.000000000000000000, 0.000000000000000000, 0.000000000000000000 ) ) ;
#835=VECTOR ( 'NONE', #3623, 39.37007874015748143 ) ;
#843=ORIENTED_EDGE ( 'NONE', *, *, #3133, .F. ) ;
#844=AXIS2_PLACEMENT_3D ( 'NONE', #5552, #1023, #6983 ) ;
#872=DIRECTION ( 'NONE',  ( 1.000000000000000000, 0.000000000000000000, 0.000000000000000000 ) ) ;
#909=LINE ( 'NONE', #5549, #7094 ) ;
#949=DIRECTION ( 'NONE',  ( -0.000000000000000000, -0.000000000000000000, -1.000000000000000000 ) ) ;
#960=ORIENTED_EDGE ( 'NONE', *, *, #3981, .F. ) ;
#963=AXIS2_PLACEMENT_3D ( 'NONE', #6501, #1241, #110 ) ;
#964=ORIENTED_EDGE ( 'NONE', *, *, #3133, .T. ) ;
#983=EDGE_CURVE ( 'NONE', #5247, #1132, #6138, .T. ) ;
#988=CIRCLE ( 'NONE', #5259, 0.2362204724409448231 ) ;
#1023=DIRECTION ( 'NONE',  ( -0.000000000000000000, -0.000000000000000000, 1.000000000000000000 ) ) ;
#1029=EDGE_CURVE ( 'NONE', #4985, #3143, #5268, .T. ) ;
#1033=EDGE_CURVE ( 'NONE', #4777, #2217, #729, .T. ) ;
#1056=CARTESIAN_POINT ( 'NONE',  ( 3.198568410424924124, 2.407012729153881203, 2.480314960629921295 ) ) ;
#1067=ADVANCED_FACE ( 'NONE', ( #7072 ), #656, .F. ) ;
#1074=VERTEX_POINT ( 'NONE', #2977 ) ;
#1076=DIRECTION ( 'NONE',  ( 0.000000000000000000, 0.000000000000000000, -1.000000000000000000 ) ) ;
#1082=DIRECTION ( 'NONE',  ( -1.000000000000000000, 0.000000000000000000, 0.000000000000000000 ) ) ;
#1097=FACE_BOUND ( 'NONE', #2604, .T. ) ;
#1100=ORIENTED_EDGE ( 'NONE', *, *, #3555, .T. ) ;
#1107=FACE_OUTER_BOUND ( 'NONE', #2197, .T. ) ;
#1121=DIRECTION ( 'NONE',  ( -0.000000000000000000, -0.000000000000000000, -1.000000000000000000 ) ) ;
#1125=FACE_OUTER_BOUND ( 'NONE', #800, .T. ) ;
#1128=DIRECTION ( 'NONE',  ( -0.000000000000000000, -0.000000000000000000, -1.000000000000000000 ) ) ;
#1132=VERTEX_POINT ( 'NONE', #5343 ) ;
#1133=AXIS2_PLACEMENT_3D ( 'NONE', #6885, #7481, #2747 ) ;
#1150=CARTESIAN_POINT ( 'NONE',  ( 3.198568410424924124, 2.407012729153881203, 0.4724409448818898127 ) ) ;
#1162=FACE_BOUND ( 'NONE', #629, .T. ) ;
#1164=ORIENTED_EDGE ( 'NONE', *, *, #4822, .T. ) ;
#1168=CARTESIAN_POINT ( 'NONE',  ( 0.7480314960629922405, 1.220472440944881942, 2.480314960629921295 ) ) ;
#1177=VECTOR ( 'NONE', #5049, 39.37007874015748143 ) ;
#1184=CIRCLE ( 'NONE', #963, 0.2362204724409448231 ) ;
#1190=CARTESIAN_POINT ( 'NONE',  ( 3.198568410424924124, 2.407012729153881203, 2.480314960629921295 ) ) ;
#1198=CARTESIAN_POINT ( 'NONE',  ( -2.834645669291338432, 0.000000000000000000, 0.4724409448818898127 ) ) ;
#1204=AXIS2_PLACEMENT_3D ( 'NONE', #454, #2271, #2874 ) ;
#1214=CARTESIAN_POINT ( 'NONE',  ( -0.5118110236220474452, 1.220472440944881942, 0.000000000000000000 ) ) ;
#1216=PRODUCT ( 'Base', 'Base', '', ( #5055 ) ) ;
#1220=AXIS2_PLACEMENT_3D ( 'NONE', #4895, #5015, #2070 ) ;
#1228=AXIS2_PLACEMENT_3D ( 'NONE', #4210, #3052, #7030 ) ;
#1232=AXIS2_PLACEMENT_3D ( 'NONE', #3485, #1076, #6420 ) ;
#1233=DIRECTION ( 'NONE',  ( -1.000000000000000000, 0.000000000000000000, 0.000000000000000000 ) ) ;
#1241=DIRECTION ( 'NONE',  ( -0.000000000000000000, -0.000000000000000000, 1.000000000000000000 ) ) ;
#1247=EDGE_CURVE ( 'NONE', #6856, #1132, #5587, .T. ) ;
#1252=CYLINDRICAL_SURFACE ( 'NONE', #5601, 1.968503937007874072 ) ;
#1258=VERTEX_POINT ( 'NONE', #3819 ) ;
#1259=VECTOR ( 'NONE', #5923, 39.37007874015748143 ) ;
#1265=LENGTH_MEASURE_WITH_UNIT ( LENGTH_MEASURE( 0.02539999999999999897 ), #1301 );
#1266=LINE ( 'NONE', #5952, #4999 ) ;
#1267=ORIENTED_EDGE ( 'NONE', *, *, #1876, .F. ) ;
#1273=DIRECTION ( 'NONE',  ( 1.000000000000000000, 0.000000000000000000, 0.000000000000000000 ) ) ;
#1301=( LENGTH_UNIT ( ) NAMED_UNIT ( * ) SI_UNIT ( $, .METRE. ) );
#1308=ORIENTED_EDGE ( 'NONE', *, *, #389, .T. ) ;
#1331=CIRCLE ( 'NONE', #6599, 1.968503937007874072 ) ;
#1341=CIRCLE ( 'NONE', #2215, 1.968503937007874072 ) ;
#1343=EDGE_CURVE ( 'NONE', #772, #1258, #2850, .T. ) ;
#1392=EDGE_CURVE ( 'NONE', #4697, #3247, #1627, .T. ) ;
#1400=ADVANCED_FACE ( 'NONE', ( #5224 ), #2249, .F. ) ;
#1413=DIRECTION ( 'NONE',  ( -1.000000000000000000, -0.000000000000000000, -0.000000000000000000 ) ) ;
#1417=EDGE_LOOP ( 'NONE', ( #658, #5953, #7045, #4091 ) ) ;
#1466=DIRECTION ( 'NONE',  ( -1.000000000000000000, 0.000000000000000000, 0.000000000000000000 ) ) ;
#1496=EDGE_CURVE ( 'NONE', #655, #6130, #7017, .T. ) ;
#1497=VECTOR ( 'NONE', #3502, 39.37007874015748143 ) ;
#1508=CARTESIAN_POINT ( 'NONE',  ( 0.9842519685039370358, 1.220472440944881942, 0.4724409448818898127 ) ) ;
#1529=VERTEX_POINT ( 'NONE', #6035 ) ;
#1535=LINE ( 'NONE', #2772, #2357 ) ;
#1554=FACE_BOUND ( 'NONE', #1577, .T. ) ;
#1577=EDGE_LOOP ( 'NONE', ( #4101, #786 ) ) ;
#1608=VECTOR ( 'NONE', #2840, 39.37007874015748143 ) ;
#1614=DIRECTION ( 'NONE',  ( -1.000000000000000000, 0.000000000000000000, 0.000000000000000000 ) ) ;
#1621=DIRECTION ( 'NONE',  ( 1.000000000000000000, 0.000000000000000000, 0.000000000000000000 ) ) ;
#1624=FACE_OUTER_BOUND ( 'NONE', #2746, .T. ) ;
#1627=LINE ( 'NONE', #4611, #6643 ) ;
#1629=CARTESIAN_POINT ( 'NONE',  ( 1.279527559055118280, 1.968503937007874072, 0.4724409448818898127 ) ) ;
#1642=ORIENTED_EDGE ( 'NONE', *, *, #2250, .F. ) ;
#1652=DIRECTION ( 'NONE',  ( -0.000000000000000000, -1.000000000000000000, 0.000000000000000000 ) ) ;
#1663=FACE_OUTER_BOUND ( 'NONE', #6270, .T. ) ;
#1668=UNCERTAINTY_MEASURE_WITH_UNIT (LENGTH_MEASURE( 1.000000000000000082E-05 ), #5254, 'distance_accuracy_value', 'NONE');
#1687=CARTESIAN_POINT ( 'NONE',  ( -2.834645669291338432, 0.000000000000000000, 2.952755905511811108 ) ) ;
#1707=ORIENTED_EDGE ( 'NONE', *, *, #1247, .F. ) ;
#1708=CARTESIAN_POINT ( 'NONE',  ( -2.834645669291338432, 0.4724409448818898127, 0.4724409448818898127 ) ) ;
#1711=VECTOR ( 'NONE', #6176, 39.37007874015748143 ) ;
#1718=AXIS2_PLACEMENT_3D ( 'NONE', #1190, #3537, #5873 ) ;
#1742=ORIENTED_EDGE ( 'NONE', *, *, #1392, .T. ) ;
#1743=VECTOR ( 'NONE', #5300, 39.37007874015748143 ) ;
#1745=DIRECTION ( 'NONE',  ( -1.000000000000000000, 0.000000000000000000, 0.000000000000000000 ) ) ;
#1752=CYLINDRICAL_SURFACE ( 'NONE', #3778, 0.2362204724409448231 ) ;
#1756=CARTESIAN_POINT ( 'NONE',  ( 1.279527559055118280, 1.968503937007874072, 2.952755905511811108 ) ) ;
#1768=FACE_BOUND ( 'NONE', #1787, .T. ) ;
#1787=EDGE_LOOP ( 'NONE', ( #5828, #2301 ) ) ;
#1816=PRODUCT_DEFINITION_CONTEXT ( 'detailed design', #5621, 'design' ) ;
#1819=DIRECTION ( 'NONE',  ( -0.000000000000000000, -0.000000000000000000, 1.000000000000000000 ) ) ;
#1823=CARTESIAN_POINT ( 'NONE',  ( -1.279527559055117836, 1.968503937007873850, 0.4724409448818898127 ) ) ;
#1825=EDGE_CURVE ( 'NONE', #1529, #4777, #447, .T. ) ;
#1829=CARTESIAN_POINT ( 'NONE',  ( 0.5118110236220474452, 1.220472440944881942, 2.480314960629921295 ) ) ;
#1837=DIRECTION ( 'NONE',  ( -0.000000000000000000, -0.000000000000000000, -1.000000000000000000 ) ) ;
#1844=AXIS2_PLACEMENT_3D ( 'NONE', #1198, #3044, #643 ) ;
#1851=AXIS2_PLACEMENT_3D ( 'NONE', #5302, #6408, #1233 ) ;
#1858=AXIS2_PLACEMENT_3D ( 'NONE', #638, #4722, #7054 ) ;
#1870=DIRECTION ( 'NONE',  ( 1.000000000000000000, 0.000000000000000000, 0.000000000000000000 ) ) ;
#1876=EDGE_CURVE ( 'NONE', #96, #4697, #2543, .T. ) ;
#1881=CARTESIAN_POINT ( 'NONE',  ( 3.198568410424924124, 2.407012729153881203, 2.480314960629921295 ) ) ;
#1903=LINE ( 'NONE', #4767, #1259 ) ;
#1921=DIRECTION ( 'NONE',  ( -1.000000000000000000, 0.000000000000000000, 0.000000000000000000 ) ) ;
#1941=VECTOR ( 'NONE', #6500, 39.37007874015748143 ) ;
#1966=ORIENTED_EDGE ( 'NONE', *, *, #7151, .F. ) ;
#1979=CARTESIAN_POINT ( 'NONE',  ( 2.834645669291338432, 0.000000000000000000, 2.952755905511811108 ) ) ;
#1980=AXIS2_PLACEMENT_3D ( 'NONE', #5484, #4282, #203 ) ;
#1982=DIRECTION ( 'NONE',  ( -1.000000000000000000, 0.000000000000000000, 0.000000000000000000 ) ) ;
#1987=DIRECTION ( 'NONE',  ( -0.000000000000000000, -0.000000000000000000, 1.000000000000000000 ) ) ;
#1994=ORIENTED_EDGE ( 'NONE', *, *, #1496, .T. ) ;
#1997=CIRCLE ( 'NONE', #5405, 0.2362204724409448231 ) ;
#2006=LINE ( 'NONE', #5605, #6194 ) ;
#2017=CARTESIAN_POINT ( 'NONE',  ( -3.198568410424924124, 2.407012729153881203, 0.000000000000000000 ) ) ;
#2028=ORIENTED_EDGE ( 'NONE', *, *, #2605, .F. ) ;
#2035=EDGE_LOOP ( 'NONE', ( #253, #4396, #7307, #7352 ) ) ;
#2040=ORIENTED_EDGE ( 'NONE', *, *, #983, .F. ) ;
#2049=ORIENTED_EDGE ( 'NONE', *, *, #3694, .T. ) ;
#2058=DIRECTION ( 'NONE',  ( -0.000000000000000000, -0.000000000000000000, -1.000000000000000000 ) ) ;
#2060=EDGE_CURVE ( 'NONE', #428, #3247, #4358, .T. ) ;
#2066=EDGE_CURVE ( 'NONE', #3143, #4985, #6096, .T. ) ;
#2070=DIRECTION ( 'NONE',  ( 0.000000000000000000, 0.000000000000000000, 1.000000000000000000 ) ) ;
#2088=ORIENTED_EDGE ( 'NONE', *, *, #5445, .T. ) ;
#2093=FACE_BOUND ( 'NONE', #6992, .T. ) ;
#2103=EDGE_CURVE ( 'NONE', #7275, #7079, #1184, .T. ) ;
#2130=CARTESIAN_POINT ( 'NONE',  ( 1.279527559055118280, 1.968503937007874072, 2.480314960629921295 ) ) ;
#2133=CYLINDRICAL_SURFACE ( 'NONE', #4313, 0.2362204724409448231 ) ;
#2134=DIRECTION ( 'NONE',  ( 0.000000000000000000, 0.000000000000000000, 1.000000000000000000 ) ) ;
#2137=CARTESIAN_POINT ( 'NONE',  ( -1.279527559055118280, 1.968503937007874072, 0.4724409448818898127 ) ) ;
#2149=ORIENTED_EDGE ( 'NONE', *, *, #2522, .F. ) ;
#2155=EDGE_CURVE ( 'NONE', #489, #5247, #2394, .T. ) ;
#2171=SHAPE_REPRESENTATION_RELATIONSHIP ( 'NONE' , 'NONE' ,  #785, #5957 ) ;
#2192=ORIENTED_EDGE ( 'NONE', *, *, #7183, .T. ) ;
#2197=EDGE_LOOP ( 'NONE', ( #4632, #5501, #2049, #2996 ) ) ;
#2198=AXIS2_PLACEMENT_3D ( 'NONE', #5282, #4790, #1921 ) ;
#2215=AXIS2_PLACEMENT_3D ( 'NONE', #5072, #2892, #7273 ) ;
#2216=CARTESIAN_POINT ( 'NONE',  ( -1.279527559055117836, 1.968503937007873850, 0.000000000000000000 ) ) ;
#2217=VERTEX_POINT ( 'NONE', #7043 ) ;
#2227=VECTOR ( 'NONE', #806, 39.37007874015748143 ) ;
#2245=VECTOR ( 'NONE', #1273, 39.37007874015748143 ) ;
#2249=CYLINDRICAL_SURFACE ( 'NONE', #3466, 1.968503937007874072 ) ;
#2250=EDGE_CURVE ( 'NONE', #1132, #6852, #1266, .T. ) ;
#2262=ORIENTED_EDGE ( 'NONE', *, *, #6405, .F. ) ;
#2270=FACE_OUTER_BOUND ( 'NONE', #5207, .T. ) ;
#2271=DIRECTION ( 'NONE',  ( -0.000000000000000000, -0.000000000000000000, -1.000000000000000000 ) ) ;
#2278=LINE ( 'NONE', #4193, #2599 ) ;
#2289=FACE_OUTER_BOUND ( 'NONE', #6723, .T. ) ;
#2293=ORIENTED_EDGE ( 'NONE', *, *, #5445, .F. ) ;
#2301=ORIENTED_EDGE ( 'NONE', *, *, #6878, .T. ) ;
#2304=CIRCLE ( 'NONE', #6585, 0.2362204724409448231 ) ;
#2330=EDGE_CURVE ( 'NONE', #6852, #5590, #4050, .T. ) ;
#2357=VECTOR ( 'NONE', #5697, 39.37007874015748143 ) ;
#2360=ORIENTED_EDGE ( 'NONE', *, *, #6264, .T. ) ;
#2367=VERTEX_POINT ( 'NONE', #1508 ) ;
#2370=EDGE_LOOP ( 'NONE', ( #1267, #2028 ) ) ;
#2394=LINE ( 'NONE', #2548, #835 ) ;
#2399=DIRECTION ( 'NONE',  ( -0.000000000000000000, 0.000000000000000000, -1.000000000000000000 ) ) ;
#2429=DIRECTION ( 'NONE',  ( 0.000000000000000000, 0.000000000000000000, 1.000000000000000000 ) ) ;
#2442=ORIENTED_EDGE ( 'NONE', *, *, #6090, .T. ) ;
#2447=DIRECTION ( 'NONE',  ( -0.000000000000000000, -0.000000000000000000, 1.000000000000000000 ) ) ;
#2480=EDGE_CURVE ( 'NONE', #2367, #4943, #2304, .T. ) ;
#2495=DIRECTION ( 'NONE',  ( -0.000000000000000000, -0.000000000000000000, 1.000000000000000000 ) ) ;
#2502=ORIENTED_EDGE ( 'NONE', *, *, #4581, .F. ) ;
#2522=EDGE_CURVE ( 'NONE', #1074, #5946, #4732, .T. ) ;
#2532=ORIENTED_EDGE ( 'NONE', *, *, #1029, .F. ) ;
#2540=VECTOR ( 'NONE', #5813, 39.37007874015748143 ) ;
#2541=LINE ( 'NONE', #6182, #373 ) ;
#2543=CIRCLE ( 'NONE', #5975, 0.2362204724409448231 ) ;
#2548=CARTESIAN_POINT ( 'NONE',  ( -1.279527559055118280, 1.968503937007874072, 2.480314960629921295 ) ) ;
#2586=CYLINDRICAL_SURFACE ( 'NONE', #4647, 0.2362204724409448231 ) ;
#2599=VECTOR ( 'NONE', #6532, 39.37007874015748143 ) ;
#2604=EDGE_LOOP ( 'NONE', ( #4956, #4865 ) ) ;
#2605=EDGE_CURVE ( 'NONE', #4697, #96, #5979, .T. ) ;
#2617=EDGE_CURVE ( 'NONE', #4891, #6130, #3653, .T. ) ;
#2646=ORIENTED_EDGE ( 'NONE', *, *, #1033, .T. ) ;
#2655=EDGE_CURVE ( 'NONE', #6508, #655, #2792, .T. ) ;
#2669=ORIENTED_EDGE ( 'NONE', *, *, #256, .F. ) ;
#2675=AXIS2_PLACEMENT_3D ( 'NONE', #6466, #1837, #2982 ) ;
#2688=MECHANICAL_DESIGN_GEOMETRIC_PRESENTATION_REPRESENTATION('',(#5996),#3429);
#2691=ORIENTED_EDGE ( 'NONE', *, *, #1876, .T. ) ;
#2701=LENGTH_MEASURE_WITH_UNIT ( LENGTH_MEASURE( 0.02539999999999999897 ), #3932 );
#2705=CARTESIAN_POINT ( 'NONE',  ( -3.198568410424924124, 2.407012729153881203, 2.480314960629921295 ) ) ;
#2707=FACE_OUTER_BOUND ( 'NONE', #1417, .T. ) ;
#2710=CARTESIAN_POINT ( 'NONE',  ( -0.9842519685039370358, 1.220472440944881942, 0.4724409448818898127 ) ) ;
#2723=ADVANCED_FACE ( 'NONE', ( #1663 ), #4667, .F. ) ;
#2741=DIRECTION ( 'NONE',  ( 1.000000000000000000, 0.000000000000000000, 0.000000000000000000 ) ) ;
#2743=DIRECTION ( 'NONE',  ( -0.000000000000000000, -0.000000000000000000, 1.000000000000000000 ) ) ;
#2746=EDGE_LOOP ( 'NONE', ( #7456, #6115, #6277, #511 ) ) ;
#2747=DIRECTION ( 'NONE',  ( -1.000000000000000000, 0.000000000000000000, 0.000000000000000000 ) ) ;
#2748=DIRECTION ( 'NONE',  ( 0.000000000000000000, 0.000000000000000000, 1.000000000000000000 ) ) ;
#2761=CARTESIAN_POINT ( 'NONE',  ( -0.7480314960629922405, 1.220472440944881942, 0.4724409448818898127 ) ) ;
#2765=ADVANCED_FACE ( 'NONE', ( #6425 ), #4131, .F. ) ;
#2772=CARTESIAN_POINT ( 'NONE',  ( 2.834645669291338432, 0.000000000000000000, 0.4724409448818898127 ) ) ;
#2792=CIRCLE ( 'NONE', #844, 0.2362204724409448231 ) ;
#2804=DIRECTION ( 'NONE',  ( 0.000000000000000000, 0.000000000000000000, 1.000000000000000000 ) ) ;
#2808=DIRECTION ( 'NONE',  ( 0.000000000000000000, 0.000000000000000000, -1.000000000000000000 ) ) ;
#2818=LINE ( 'NONE', #3326, #6249 ) ;
#2840=DIRECTION ( 'NONE',  ( -0.000000000000000000, -0.000000000000000000, -1.000000000000000000 ) ) ;
#2850=CIRCLE ( 'NONE', #5428, 1.968503937007874072 ) ;
#2874=DIRECTION ( 'NONE',  ( -1.000000000000000000, 0.000000000000000000, 0.000000000000000000 ) ) ;
#2883=FACE_OUTER_BOUND ( 'NONE', #6810, .T. ) ;
#2892=DIRECTION ( 'NONE',  ( -0.000000000000000000, -0.000000000000000000, -1.000000000000000000 ) ) ;
#2904=ORIENTED_EDGE ( 'NONE', *, *, #4861, .T. ) ;
#2906=VECTOR ( 'NONE', #1128, 39.37007874015748143 ) ;
#2913=ORIENTED_EDGE ( 'NONE', *, *, #3694, .F. ) ;
#2918=LINE ( 'NONE', #5198, #1497 ) ;
#2927=CARTESIAN_POINT ( 'NONE',  ( -2.834645669291338432, 0.4724409448818890911, 0.4724409448818902013 ) ) ;
#2930=ORIENTED_EDGE ( 'NONE', *, *, #3645, .T. ) ;
#2932=VERTEX_POINT ( 'NONE', #7096 ) ;
#2935=DIRECTION ( 'NONE',  ( -0.000000000000000000, -0.000000000000000000, 1.000000000000000000 ) ) ;
#2936=ORIENTED_EDGE ( 'NONE', *, *, #6224, .F. ) ;
#2955=ORIENTED_EDGE ( 'NONE', *, *, #6126, .F. ) ;
#2964=CARTESIAN_POINT ( 'NONE',  ( -0.9842519685039370358, 1.220472440944881942, 2.480314960629921295 ) ) ;
#2969=DIRECTION ( 'NONE',  ( 0.000000000000000000, 0.000000000000000000, 1.000000000000000000 ) ) ;
#2973=CARTESIAN_POINT ( 'NONE',  ( -0.7480314960629922405, 1.220472440944881942, 2.480314960629921295 ) ) ;
#2977=CARTESIAN_POINT ( 'NONE',  ( -1.279527559055117836, 1.968503937007873850, 0.4724409448818898127 ) ) ;
#2982=DIRECTION ( 'NONE',  ( -1.000000000000000000, 0.000000000000000000, 0.000000000000000000 ) ) ;
#2991=ORIENTED_EDGE ( 'NONE', *, *, #3369, .F. ) ;
#2996=ORIENTED_EDGE ( 'NONE', *, *, #7375, .T. ) ;
#3000=CARTESIAN_POINT ( 'NONE',  ( 0.9842519685039370358, 1.220472440944881942, 2.480314960629921295 ) ) ;
#3001=LINE ( 'NONE', #679, #2245 ) ;
#3021=AXIS2_PLACEMENT_3D ( 'NONE', #4773, #5307, #5781 ) ;
#3039=DIRECTION ( 'NONE',  ( 0.000000000000000000, 1.000000000000000000, 0.000000000000000000 ) ) ;
#3044=DIRECTION ( 'NONE',  ( 0.000000000000000000, 1.000000000000000000, 0.000000000000000000 ) ) ;
#3052=DIRECTION ( 'NONE',  ( 0.000000000000000000, 0.000000000000000000, 1.000000000000000000 ) ) ;
#3077=CIRCLE ( 'NONE', #1858, 1.968503937007874072 ) ;
#3117=CARTESIAN_POINT ( 'NONE',  ( 1.279527559055118280, 1.968503937007874072, 2.480314960629921295 ) ) ;
#3133=EDGE_CURVE ( 'NONE', #2367, #3143, #796, .T. ) ;
#3143=VERTEX_POINT ( 'NONE', #4094 ) ;
#3174=FACE_OUTER_BOUND ( 'NONE', #6464, .T. ) ;
#3191=ADVANCED_FACE ( 'NONE', ( #1107 ), #1752, .F. ) ;
#3196=DIRECTION ( 'NONE',  ( 0.000000000000000000, 1.000000000000000000, 0.000000000000000000 ) ) ;
#3229=ORIENTED_EDGE ( 'NONE', *, *, #5325, .T. ) ;
#3247=VERTEX_POINT ( 'NONE', #1214 ) ;
#3248=PRODUCT_DEFINITION_FORMATION_WITH_SPECIFIED_SOURCE ( 'ANY', '', #1216, .NOT_KNOWN. ) ;
#3278=CARTESIAN_POINT ( 'NONE',  ( -0.7480314960629922405, 1.220472440944881942, 0.4724409448818898127 ) ) ;
#3319=DIRECTION ( 'NONE',  ( -1.000000000000000000, 0.000000000000000000, 0.000000000000000000 ) ) ;
#3323=VERTEX_POINT ( 'NONE', #1756 ) ;
#3326=CARTESIAN_POINT ( 'NONE',  ( 0.5118110236220474452, 1.220472440944881942, 0.4724409448818898127 ) ) ;
#3344=ORIENTED_EDGE ( 'NONE', *, *, #2155, .T. ) ;
#3350=PLANE ( 'NONE',  #7463 ) ;
#3369=EDGE_CURVE ( 'NONE', #489, #3323, #6831, .T. ) ;
#3412=VECTOR ( 'NONE', #190, 39.37007874015748143 ) ;
#3429=( GEOMETRIC_REPRESENTATION_CONTEXT ( 3 ) GLOBAL_UNCERTAINTY_ASSIGNED_CONTEXT ( ( #1668 ) ) GLOBAL_UNIT_ASSIGNED_CONTEXT ( ( #5254, #3527, #5367 ) ) REPRESENTATION_CONTEXT ( 'NONE', 'WORKASPACE' ) );
#3438=AXIS2_PLACEMENT_3D ( 'NONE', #6648, #792, #4388 ) ;
#3447=EDGE_LOOP ( 'NONE', ( #5235, #2262 ) ) ;
#3448=CARTESIAN_POINT ( 'NONE',  ( -3.198568410424924124, 2.407012729153881203, 2.480314960629921295 ) ) ;
#3450=EDGE_LOOP ( 'NONE', ( #4203, #4244 ) ) ;
#3466=AXIS2_PLACEMENT_3D ( 'NONE', #1150, #1121, #6908 ) ;
#3476=LINE ( 'NONE', #5929, #2540 ) ;
#3485=CARTESIAN_POINT ( 'NONE',  ( -3.198568410424924124, 2.407012729153881203, 2.952755905511811108 ) ) ;
#3500=DIRECTION ( 'NONE',  ( 1.000000000000000000, 0.000000000000000000, 0.000000000000000000 ) ) ;
#3502=DIRECTION ( 'NONE',  ( -0.000000000000000000, -0.000000000000000000, 1.000000000000000000 ) ) ;
#3527=( NAMED_UNIT ( * ) PLANE_ANGLE_UNIT ( ) SI_UNIT ( $, .RADIAN. ) );
#3537=DIRECTION ( 'NONE',  ( 0.000000000000000000, -0.000000000000000000, 1.000000000000000000 ) ) ;
#3550=PLANE ( 'NONE',  #6753 ) ;
#3554=EDGE_LOOP ( 'NONE', ( #3229, #5593, #5652, #6776, #7496, #3823 ) ) ;
#3555=EDGE_CURVE ( 'NONE', #321, #6807, #2541, .T. ) ;
#3560=CARTESIAN_POINT ( 'NONE',  ( 2.834645669291338876, 0.4724409448818890911, 2.480314960629921295 ) ) ;
#3584=CARTESIAN_POINT ( 'NONE',  ( 2.834645669291338432, 0.000000000000000000, 0.000000000000000000 ) ) ;
#3623=DIRECTION ( 'NONE',  ( -1.000000000000000000, -0.000000000000000000, 0.000000000000000000 ) ) ;
#3640=ORIENTED_EDGE ( 'NONE', *, *, #6117, .T. ) ;
#3645=EDGE_CURVE ( 'NONE', #5971, #3323, #122, .T. ) ;
#3653=CIRCLE ( 'NONE', #361, 0.2362204724409448231 ) ;
#3656=EDGE_CURVE ( 'NONE', #5946, #5590, #1331, .T. ) ;
#3688=AXIS2_PLACEMENT_3D ( 'NONE', #5386, #1819, #5811 ) ;
#3694=EDGE_CURVE ( 'NONE', #7275, #4992, #220, .T. ) ;
#3697=ORIENTED_EDGE ( 'NONE', *, *, #7432, .T. ) ;
#3734=ADVANCED_FACE ( 'NONE', ( #4599 ), #5078, .F. ) ;
#3735=DIRECTION ( 'NONE',  ( 0.000000000000000000, 0.000000000000000000, -1.000000000000000000 ) ) ;
#3778=AXIS2_PLACEMENT_3D ( 'NONE', #6968, #5283, #552 ) ;
#3803=ORIENTED_EDGE ( 'NONE', *, *, #5197, .F. ) ;
#3805=ORIENTED_EDGE ( 'NONE', *, *, #2480, .T. ) ;
#3817=VECTOR ( 'NONE', #2495, 39.37007874015748143 ) ;
#3819=CARTESIAN_POINT ( 'NONE',  ( 1.279527559055118280, 1.968503937007874072, 0.4724409448818898127 ) ) ;
#3823=ORIENTED_EDGE ( 'NONE', *, *, #2330, .T. ) ;
#3841=ADVANCED_FACE ( 'NONE', ( #5658 ), #6296, .F. ) ;
#3849=CARTESIAN_POINT ( 'NONE',  ( 3.198568410424924124, 2.407012729153881203, 2.952755905511811108 ) ) ;
#3868=DIRECTION ( 'NONE',  ( 0.000000000000000000, -0.000000000000000000, -1.000000000000000000 ) ) ;
#3888=DIRECTION ( 'NONE',  ( 1.000000000000000000, 0.000000000000000000, 0.000000000000000000 ) ) ;
#3890=DIRECTION ( 'NONE',  ( -1.000000000000000000, 0.000000000000000000, 0.000000000000000000 ) ) ;
#3898=LINE ( 'NONE', #1629, #830 ) ;
#3907=EDGE_LOOP ( 'NONE', ( #3803, #3989, #6084, #2442 ) ) ;
#3920=ORIENTED_EDGE ( 'NONE', *, *, #2655, .F. ) ;
#3928=MANIFOLD_SOLID_BREP ( 'Boss-Extrude2', #4682 ) ;
#3931=CARTESIAN_POINT ( 'NONE',  ( 3.198568410424924124, 2.407012729153881203, 0.4724409448818898127 ) ) ;
#3932=( LENGTH_UNIT ( ) NAMED_UNIT ( * ) SI_UNIT ( $, .METRE. ) );
#3972=( NAMED_UNIT ( * ) PLANE_ANGLE_UNIT ( ) SI_UNIT ( $, .RADIAN. ) );
#3981=EDGE_CURVE ( 'NONE', #2932, #5946, #2006, .T. ) ;
#3989=ORIENTED_EDGE ( 'NONE', *, *, #6117, .F. ) ;
#4036=CARTESIAN_POINT ( 'NONE',  ( 0.5118110236220474452, 1.220472440944881942, 2.480314960629921295 ) ) ;
#4046=AXIS2_PLACEMENT_3D ( 'NONE', #5054, #2748, #5090 ) ;
#4050=LINE ( 'NONE', #1708, #2906 ) ;
#4063=EDGE_LOOP ( 'NONE', ( #5151, #5936, #7425, #2913 ) ) ;
#4087=ORIENTED_EDGE ( 'NONE', *, *, #1247, .T. ) ;
#4090=DIRECTION ( 'NONE',  ( -1.000000000000000000, 0.000000000000000000, 0.000000000000000000 ) ) ;
#4091=ORIENTED_EDGE ( 'NONE', *, *, #2522, .T. ) ;
#4094=CARTESIAN_POINT ( 'NONE',  ( 0.9842519685039370358, 1.220472440944881942, 0.000000000000000000 ) ) ;
#4101=ORIENTED_EDGE ( 'NONE', *, *, #2617, .F. ) ;
#4108=FACE_OUTER_BOUND ( 'NONE', #7290, .T. ) ;
#4109=DIRECTION ( 'NONE',  ( -0.000000000000000000, -0.000000000000000000, 1.000000000000000000 ) ) ;
#4131=CYLINDRICAL_SURFACE ( 'NONE', #2675, 0.2362204724409448231 ) ;
#4143=CARTESIAN_POINT ( 'NONE',  ( -0.7480314960629922405, 1.220472440944881942, 2.952755905511811108 ) ) ;
#4187=ORIENTED_EDGE ( 'NONE', *, *, #5052, .F. ) ;
#4189=AXIS2_PLACEMENT_3D ( 'NONE', #4686, #2429, #5263 ) ;
#4193=CARTESIAN_POINT ( 'NONE',  ( -1.279527559055117836, 1.968503937007873850, 2.480314960629921295 ) ) ;
#4203=ORIENTED_EDGE ( 'NONE', *, *, #2655, .T. ) ;
#4208=ADVANCED_FACE ( 'NONE', ( #5857 ), #1252, .F. ) ;
#4210=CARTESIAN_POINT ( 'NONE',  ( 0.7480314960629922405, 1.220472440944881942, 0.000000000000000000 ) ) ;
#4212=DIRECTION ( 'NONE',  ( 1.000000000000000000, 0.000000000000000000, 0.000000000000000000 ) ) ;
#4213=ORIENTED_EDGE ( 'NONE', *, *, #389, .F. ) ;
#4244=ORIENTED_EDGE ( 'NONE', *, *, #4246, .T. ) ;
#4246=EDGE_CURVE ( 'NONE', #655, #6508, #7044, .T. ) ;
#4251=ORIENTED_EDGE ( 'NONE', *, *, #6837, .T. ) ;
#4276=DIRECTION ( 'NONE',  ( 0.000000000000000000, 0.000000000000000000, 1.000000000000000000 ) ) ;
#4281=VECTOR ( 'NONE', #6457, 39.37007874015748143 ) ;
#4282=DIRECTION ( 'NONE',  ( 0.000000000000000000, -1.000000000000000000, 0.000000000000000000 ) ) ;
#4313=AXIS2_PLACEMENT_3D ( 'NONE', #6796, #5158, #6755 ) ;
#4328=CARTESIAN_POINT ( 'NONE',  ( -0.5118110236220474452, 1.220472440944881942, 2.480314960629921295 ) ) ;
#4358=CIRCLE ( 'NONE', #5353, 0.2362204724409448231 ) ;
#4388=DIRECTION ( 'NONE',  ( -1.000000000000000000, 0.000000000000000000, 0.000000000000000000 ) ) ;
#4396=ORIENTED_EDGE ( 'NONE', *, *, #4861, .F. ) ;
#4403=ORIENTED_EDGE ( 'NONE', *, *, #4246, .F. ) ;
#4406=ORIENTED_EDGE ( 'NONE', *, *, #6264, .F. ) ;
#4425=( GEOMETRIC_REPRESENTATION_CONTEXT ( 3 ) GLOBAL_UNCERTAINTY_ASSIGNED_CONTEXT ( ( #7050 ) ) GLOBAL_UNIT_ASSIGNED_CONTEXT ( ( #6262, #3972, #6797 ) ) REPRESENTATION_CONTEXT ( 'NONE', 'WORKASPACE' ) );
#4448=ORIENTED_EDGE ( 'NONE', *, *, #6050, .F. ) ;
#4505=DIRECTION ( 'NONE',  ( -1.000000000000000000, 0.000000000000000000, 0.000000000000000000 ) ) ;
#4545=AXIS2_PLACEMENT_3D ( 'NONE', #3448, #479, #5819 ) ;
#4549=CIRCLE ( 'NONE', #1232, 1.968503937007874072 ) ;
#4581=EDGE_CURVE ( 'NONE', #4777, #6862, #3476, .T. ) ;
#4599=FACE_OUTER_BOUND ( 'NONE', #7388, .T. ) ;
#4605=LINE ( 'NONE', #5252, #1608 ) ;
#4611=CARTESIAN_POINT ( 'NONE',  ( -0.5118110236220474452, 1.220472440944881942, 0.4724409448818898127 ) ) ;
#4621=DIMENSIONAL_EXPONENTS ( 1.000000000000000000, 0.000000000000000000, 0.000000000000000000, 0.000000000000000000, 0.000000000000000000, 0.000000000000000000, 0.000000000000000000 ) ;
#4626=ADVANCED_FACE ( 'NONE', ( #6499 ), #111, .F. ) ;
#4632=ORIENTED_EDGE ( 'NONE', *, *, #6678, .F. ) ;
#4638=CARTESIAN_POINT ( 'NONE',  ( 0.9842519685039370358, 1.220472440944881942, 2.480314960629921295 ) ) ;
#4646=CARTESIAN_POINT ( 'NONE',  ( 0.7480314960629922405, 1.220472440944881942, 2.952755905511811108 ) ) ;
#4647=AXIS2_PLACEMENT_3D ( 'NONE', #4925, #2058, #1982 ) ;
#4667=CYLINDRICAL_SURFACE ( 'NONE', #2198, 0.2362204724409448231 ) ;
#4680=DIRECTION ( 'NONE',  ( -1.000000000000000000, 0.000000000000000000, 0.000000000000000000 ) ) ;
#4682=CLOSED_SHELL ( 'NONE', ( #4626, #6343, #2765, #7471, #6360, #5631, #660, #1400, #1067, #6041, #3841, #7374, #3734, #2723, #5628, #7010, #234, #4208, #7048, #4823, #7470, #3191 ) ) ;
#4686=CARTESIAN_POINT ( 'NONE',  ( 0.7480314960629922405, 1.220472440944881942, 0.4724409448818898127 ) ) ;
#4697=VERTEX_POINT ( 'NONE', #7253 ) ;
#4722=DIRECTION ( 'NONE',  ( -0.000000000000000000, -0.000000000000000000, -1.000000000000000000 ) ) ;
#4732=LINE ( 'NONE', #1823, #1941 ) ;
#4767=CARTESIAN_POINT ( 'NONE',  ( -1.279527559055118280, 1.968503937007874072, 2.952755905511811108 ) ) ;
#4773=CARTESIAN_POINT ( 'NONE',  ( -0.7480314960629922405, 1.220472440944881942, 2.480314960629921295 ) ) ;
#4777=VERTEX_POINT ( 'NONE', #344 ) ;
#4788=LINE ( 'NONE', #3560, #3817 ) ;
#4790=DIRECTION ( 'NONE',  ( -0.000000000000000000, -0.000000000000000000, -1.000000000000000000 ) ) ;
#4822=EDGE_CURVE ( 'NONE', #6856, #489, #4965, .T. ) ;
#4823=ADVANCED_FACE ( 'NONE', ( #7439 ), #379, .F. ) ;
#4824=EDGE_CURVE ( 'NONE', #1258, #1074, #462, .T. ) ;
#4827=DIRECTION ( 'NONE',  ( -0.000000000000000000, -1.000000000000000000, -0.000000000000000000 ) ) ;
#4847=DIRECTION ( 'NONE',  ( 0.000000000000000000, 0.000000000000000000, 1.000000000000000000 ) ) ;
#4861=EDGE_CURVE ( 'NONE', #1258, #2932, #3898, .T. ) ;
#4863=AXIS2_PLACEMENT_3D ( 'NONE', #1056, #6879, #5629 ) ;
#4865=ORIENTED_EDGE ( 'NONE', *, *, #2066, .T. ) ;
#4869=SHAPE_DEFINITION_REPRESENTATION ( #270, #785 ) ;
#4873=ORIENTED_EDGE ( 'NONE', *, *, #7183, .F. ) ;
#4889=CARTESIAN_POINT ( 'NONE',  ( 0.7480314960629922405, 1.220472440944881942, 2.952755905511811108 ) ) ;
#4891=VERTEX_POINT ( 'NONE', #5667 ) ;
#4895=CARTESIAN_POINT ( 'NONE',  ( -1.279527559055118280, 1.968503937007874072, 2.480314960629921295 ) ) ;
#4924=VECTOR ( 'NONE', #5998, 39.37007874015748143 ) ;
#4925=CARTESIAN_POINT ( 'NONE',  ( 0.7480314960629922405, 1.220472440944881942, 0.4724409448818898127 ) ) ;
#4943=VERTEX_POINT ( 'NONE', #7507 ) ;
#4956=ORIENTED_EDGE ( 'NONE', *, *, #1029, .T. ) ;
#4957=DIRECTION ( 'NONE',  ( -0.000000000000000000, -0.000000000000000000, 1.000000000000000000 ) ) ;
#4965=CIRCLE ( 'NONE', #4863, 1.968503937007874072 ) ;
#4985=VERTEX_POINT ( 'NONE', #563 ) ;
#4992=VERTEX_POINT ( 'NONE', #5301 ) ;
#4999=VECTOR ( 'NONE', #671, 39.37007874015748143 ) ;
#5010=EDGE_CURVE ( 'NONE', #6130, #4891, #6376, .T. ) ;
#5015=DIRECTION ( 'NONE',  ( 0.000000000000000000, -1.000000000000000000, 0.000000000000000000 ) ) ;
#5032=CARTESIAN_POINT ( 'NONE',  ( -0.5118110236220474452, 1.220472440944881942, 2.480314960629921295 ) ) ;
#5034=ORIENTED_EDGE ( 'NONE', *, *, #3369, .T. ) ;
#5049=DIRECTION ( 'NONE',  ( -1.000000000000000000, -0.000000000000000000, -0.000000000000000000 ) ) ;
#5050=CYLINDRICAL_SURFACE ( 'NONE', #1851, 1.968503937007874072 ) ;
#5052=EDGE_CURVE ( 'NONE', #6807, #2932, #3077, .T. ) ;
#5054=CARTESIAN_POINT ( 'NONE',  ( -0.7480314960629922405, 1.220472440944881942, 0.000000000000000000 ) ) ;
#5055=PRODUCT_CONTEXT ( 'NONE', #673, 'mechanical' ) ;
#5062=ORIENTED_EDGE ( 'NONE', *, *, #6837, .F. ) ;
#5072=CARTESIAN_POINT ( 'NONE',  ( -3.198568410424924124, 2.407012729153881203, 0.4724409448818898127 ) ) ;
#5078=CYLINDRICAL_SURFACE ( 'NONE', #1204, 0.2362204724409448231 ) ;
#5083=CARTESIAN_POINT ( 'NONE',  ( -2.834645669291338432, 0.4724409448818890911, 2.480314960629921295 ) ) ;
#5087=CARTESIAN_POINT ( 'NONE',  ( 2.834645669291338876, 0.4724409448818890911, 2.952755905511811108 ) ) ;
#5088=ORIENTED_EDGE ( 'NONE', *, *, #1825, .T. ) ;
#5090=DIRECTION ( 'NONE',  ( -1.000000000000000000, 0.000000000000000000, 0.000000000000000000 ) ) ;
#5108=LINE ( 'NONE', #5032, #1711 ) ;
#5122=DIRECTION ( 'NONE',  ( -0.000000000000000000, -0.000000000000000000, -1.000000000000000000 ) ) ;
#5130=FACE_BOUND ( 'NONE', #3447, .T. ) ;
#5151=ORIENTED_EDGE ( 'NONE', *, *, #6878, .F. ) ;
#5158=DIRECTION ( 'NONE',  ( -0.000000000000000000, -0.000000000000000000, 1.000000000000000000 ) ) ;
#5166=AXIS2_PLACEMENT_3D ( 'NONE', #418, #2134, #2741 ) ;
#5175=AXIS2_PLACEMENT_3D ( 'NONE', #5177, #7487, #3868 ) ;
#5177=CARTESIAN_POINT ( 'NONE',  ( -2.834645669291338432, 0.4724409448818890911, 8.169257281319195485 ) ) ;
#5197=EDGE_CURVE ( 'NONE', #5932, #1529, #4549, .T. ) ;
#5198=CARTESIAN_POINT ( 'NONE',  ( -2.834645669291338432, 0.4724409448818898127, 2.480314960629921295 ) ) ;
#5207=EDGE_LOOP ( 'NONE', ( #1100, #6243, #2293, #6815, #2936, #1308 ) ) ;
#5224=FACE_OUTER_BOUND ( 'NONE', #2035, .T. ) ;
#5235=ORIENTED_EDGE ( 'NONE', *, *, #7375, .F. ) ;
#5237=CARTESIAN_POINT ( 'NONE',  ( 2.834645669291338432, 0.000000000000000000, 2.952755905511811108 ) ) ;
#5247=VERTEX_POINT ( 'NONE', #6289 ) ;
#5251=AXIS2_PLACEMENT_3D ( 'NONE', #3849, #3735, #7277 ) ;
#5252=CARTESIAN_POINT ( 'NONE',  ( 2.834645669291338876, 0.4724409448818890911, 0.4724409448818898127 ) ) ;
#5254=( CONVERSION_BASED_UNIT ( 'INCH', #1265 ) LENGTH_UNIT ( ) NAMED_UNIT ( #4621 ) );
#5259=AXIS2_PLACEMENT_3D ( 'NONE', #2973, #6991, #1745 ) ;
#5263=DIRECTION ( 'NONE',  ( 1.000000000000000000, 0.000000000000000000, 0.000000000000000000 ) ) ;
#5268=CIRCLE ( 'NONE', #1228, 0.2362204724409448231 ) ;
#5281=EDGE_CURVE ( 'NONE', #6856, #5971, #4788, .T. ) ;
#5282=CARTESIAN_POINT ( 'NONE',  ( -0.7480314960629922405, 1.220472440944881942, 0.4724409448818898127 ) ) ;
#5283=DIRECTION ( 'NONE',  ( -0.000000000000000000, -0.000000000000000000, 1.000000000000000000 ) ) ;
#5296=ORIENTED_EDGE ( 'NONE', *, *, #2060, .F. ) ;
#5300=DIRECTION ( 'NONE',  ( -0.000000000000000000, -0.000000000000000000, 1.000000000000000000 ) ) ;
#5301=CARTESIAN_POINT ( 'NONE',  ( -0.9842519685039370358, 1.220472440944881942, 2.952755905511811108 ) ) ;
#5302=CARTESIAN_POINT ( 'NONE',  ( -3.198568410424924124, 2.407012729153881203, 0.4724409448818898127 ) ) ;
#5307=DIRECTION ( 'NONE',  ( -0.000000000000000000, -0.000000000000000000, 1.000000000000000000 ) ) ;
#5313=CARTESIAN_POINT ( 'NONE',  ( 2.834645669291338876, 0.4724409448818890911, 0.000000000000000000 ) ) ;
#5325=EDGE_CURVE ( 'NONE', #5590, #2217, #5902, .T. ) ;
#5343=CARTESIAN_POINT ( 'NONE',  ( -2.834645669291338432, 0.4724409448818898127, 2.480314960629921295 ) ) ;
#5350=DIRECTION ( 'NONE',  ( -1.000000000000000000, 0.000000000000000000, 0.000000000000000000 ) ) ;
#5353=AXIS2_PLACEMENT_3D ( 'NONE', #113, #4276, #268 ) ;
#5367=( NAMED_UNIT ( * ) SI_UNIT ( $, .STERADIAN. ) SOLID_ANGLE_UNIT ( ) );
#5386=CARTESIAN_POINT ( 'NONE',  ( -0.7480314960629922405, 1.220472440944881942, 2.952755905511811108 ) ) ;
#5405=AXIS2_PLACEMENT_3D ( 'NONE', #4143, #631, #4680 ) ;
#5426=CARTESIAN_POINT ( 'NONE',  ( -0.9842519685039370358, 1.220472440944881942, 0.4724409448818898127 ) ) ;
#5428=AXIS2_PLACEMENT_3D ( 'NONE', #6227, #307, #4505 ) ;
#5434=CARTESIAN_POINT ( 'NONE',  ( 0.9842519685039370358, 1.220472440944881942, 0.4724409448818898127 ) ) ;
#5445=EDGE_CURVE ( 'NONE', #6856, #772, #125, .T. ) ;
#5484=CARTESIAN_POINT ( 'NONE',  ( -1.279527559055118280, 1.968503937007874072, 0.4724409448818898127 ) ) ;
#5488=AXIS2_PLACEMENT_3D ( 'NONE', #2705, #2743, #1466 ) ;
#5501=ORIENTED_EDGE ( 'NONE', *, *, #2103, .F. ) ;
#5504=VECTOR ( 'NONE', #5657, 39.37007874015748143 ) ;
#5544=EDGE_LOOP ( 'NONE', ( #6893, #6051, #1164, #5034 ) ) ;
#5549=CARTESIAN_POINT ( 'NONE',  ( -2.834645669291338432, 0.4724409448818890911, 0.4724409448818902013 ) ) ;
#5552=CARTESIAN_POINT ( 'NONE',  ( 0.7480314960629922405, 1.220472440944881942, 2.480314960629921295 ) ) ;
#5587=LINE ( 'NONE', #5083, #6632 ) ;
#5590=VERTEX_POINT ( 'NONE', #545 ) ;
#5593=ORIENTED_EDGE ( 'NONE', *, *, #1033, .F. ) ;
#5601=AXIS2_PLACEMENT_3D ( 'NONE', #1881, #2935, #4090 ) ;
#5605=CARTESIAN_POINT ( 'NONE',  ( -1.279527559055118280, 1.968503937007874072, 0.000000000000000000 ) ) ;
#5621=APPLICATION_CONTEXT ( 'automotive_design' ) ;
#5628=ADVANCED_FACE ( 'NONE', ( #2289 ), #6956, .F. ) ;
#5629=DIRECTION ( 'NONE',  ( -1.000000000000000000, 0.000000000000000000, 0.000000000000000000 ) ) ;
#5630=DIRECTION ( 'NONE',  ( 0.000000000000000000, 0.000000000000000000, 1.000000000000000000 ) ) ;
#5631=ADVANCED_FACE ( 'NONE', ( #1097, #6201, #1162 ), #3550, .T. ) ;
#5640=ORIENTED_EDGE ( 'NONE', *, *, #7151, .T. ) ;
#5652=ORIENTED_EDGE ( 'NONE', *, *, #1825, .F. ) ;
#5657=DIRECTION ( 'NONE',  ( -0.000000000000000000, -0.000000000000000000, 1.000000000000000000 ) ) ;
#5658=FACE_OUTER_BOUND ( 'NONE', #3554, .T. ) ;
#5664=VECTOR ( 'NONE', #4827, 39.37007874015748143 ) ;
#5667=CARTESIAN_POINT ( 'NONE',  ( 0.5118110236220474452, 1.220472440944881942, 2.952755905511811108 ) ) ;
#5697=DIRECTION ( 'NONE',  ( -0.000000000000000000, -0.000000000000000000, -1.000000000000000000 ) ) ;
#5781=DIRECTION ( 'NONE',  ( -1.000000000000000000, 0.000000000000000000, 0.000000000000000000 ) ) ;
#5811=DIRECTION ( 'NONE',  ( -1.000000000000000000, 0.000000000000000000, 0.000000000000000000 ) ) ;
#5813=DIRECTION ( 'NONE',  ( 1.000000000000000000, 0.000000000000000000, 0.000000000000000000 ) ) ;
#5819=DIRECTION ( 'NONE',  ( 1.000000000000000000, 0.000000000000000000, 0.000000000000000000 ) ) ;
#5828=ORIENTED_EDGE ( 'NONE', *, *, #2103, .T. ) ;
#5834=AXIS2_PLACEMENT_3D ( 'NONE', #1168, #2447, #4212 ) ;
#5847=EDGE_LOOP ( 'NONE', ( #6427, #3920, #4251, #821 ) ) ;
#5857=FACE_OUTER_BOUND ( 'NONE', #5544, .T. ) ;
#5873=DIRECTION ( 'NONE',  ( -1.000000000000000000, 0.000000000000000000, 0.000000000000000000 ) ) ;
#5901=ORIENTED_EDGE ( 'NONE', *, *, #3555, .F. ) ;
#5902=LINE ( 'NONE', #6424, #5664 ) ;
#5923=DIRECTION ( 'NONE',  ( -1.000000000000000000, -0.000000000000000000, 0.000000000000000000 ) ) ;
#5929=CARTESIAN_POINT ( 'NONE',  ( -2.834645669291338432, 0.000000000000000000, 2.952755905511811108 ) ) ;
#5932=VERTEX_POINT ( 'NONE', #381 ) ;
#5936=ORIENTED_EDGE ( 'NONE', *, *, #6678, .T. ) ;
#5946=VERTEX_POINT ( 'NONE', #2216 ) ;
#5952=CARTESIAN_POINT ( 'NONE',  ( -2.834645669291338432, 0.4724409448818890911, 8.169257281319195485 ) ) ;
#5953=ORIENTED_EDGE ( 'NONE', *, *, #2330, .F. ) ;
#5957=ADVANCED_BREP_SHAPE_REPRESENTATION ( '', ( #3928, #5166 ), #4425 ) ;
#5960=CARTESIAN_POINT ( 'NONE',  ( 0.9842519685039370358, 1.220472440944881942, 2.952755905511811108 ) ) ;
#5971=VERTEX_POINT ( 'NONE', #5087 ) ;
#5975=AXIS2_PLACEMENT_3D ( 'NONE', #2761, #2969, #1614 ) ;
#5979=CIRCLE ( 'NONE', #6945, 0.2362204724409448231 ) ;
#5996=STYLED_ITEM('',(#7559),#3928);
#5998=DIRECTION ( 'NONE',  ( -0.000000000000000000, -0.000000000000000000, -1.000000000000000000 ) ) ;
#6012=CARTESIAN_POINT ( 'NONE',  ( 2.834645669291338876, 0.4724409448818890911, 2.480314960629921295 ) ) ;
#6022=ORIENTED_EDGE ( 'NONE', *, *, #5325, .F. ) ;
#6025=EDGE_LOOP ( 'NONE', ( #5901, #2955, #6022, #6783, #960, #4187 ) ) ;
#6029=PRODUCT_DEFINITION ( 'UNKNOWN', '', #3248, #1816 ) ;
#6035=CARTESIAN_POINT ( 'NONE',  ( -2.834645669291338432, 0.4724409448818898127, 2.952755905511811108 ) ) ;
#6041=ADVANCED_FACE ( 'NONE', ( #2707 ), #5050, .F. ) ;
#6050=EDGE_CURVE ( 'NONE', #4943, #2367, #294, .T. ) ;
#6051=ORIENTED_EDGE ( 'NONE', *, *, #5281, .F. ) ;
#6063=ORIENTED_EDGE ( 'NONE', *, *, #2060, .T. ) ;
#6084=ORIENTED_EDGE ( 'NONE', *, *, #983, .T. ) ;
#6090=EDGE_CURVE ( 'NONE', #1132, #1529, #2918, .T. ) ;
#6096=CIRCLE ( 'NONE', #6829, 0.2362204724409448231 ) ;
#6112=FACE_OUTER_BOUND ( 'NONE', #809, .T. ) ;
#6115=ORIENTED_EDGE ( 'NONE', *, *, #1343, .T. ) ;
#6117=EDGE_CURVE ( 'NONE', #5247, #5932, #2278, .T. ) ;
#6126=EDGE_CURVE ( 'NONE', #2217, #321, #3001, .T. ) ;
#6130=VERTEX_POINT ( 'NONE', #5960 ) ;
#6138=CIRCLE ( 'NONE', #4545, 1.968503937007874072 ) ;
#6176=DIRECTION ( 'NONE',  ( -0.000000000000000000, -0.000000000000000000, 1.000000000000000000 ) ) ;
#6182=CARTESIAN_POINT ( 'NONE',  ( 2.834645669291338432, 0.000000000000000000, 0.000000000000000000 ) ) ;
#6185=FACE_BOUND ( 'NONE', #2370, .T. ) ;
#6194=VECTOR ( 'NONE', #1413, 39.37007874015748143 ) ;
#6199=ORIENTED_EDGE ( 'NONE', *, *, #4822, .F. ) ;
#6201=FACE_OUTER_BOUND ( 'NONE', #6025, .T. ) ;
#6224=EDGE_CURVE ( 'NONE', #6862, #5971, #716, .T. ) ;
#6227=CARTESIAN_POINT ( 'NONE',  ( 3.198568410424924124, 2.407012729153881203, 0.4724409448818898127 ) ) ;
#6243=ORIENTED_EDGE ( 'NONE', *, *, #664, .F. ) ;
#6249=VECTOR ( 'NONE', #7368, 39.37007874015748143 ) ;
#6262=( CONVERSION_BASED_UNIT ( 'INCH', #2701 ) LENGTH_UNIT ( ) NAMED_UNIT ( #490 ) );
#6264=EDGE_CURVE ( 'NONE', #96, #428, #749, .T. ) ;
#6270=EDGE_LOOP ( 'NONE', ( #699, #255, #2360, #1966 ) ) ;
#6277=ORIENTED_EDGE ( 'NONE', *, *, #4824, .T. ) ;
#6281=ORIENTED_EDGE ( 'NONE', *, *, #3981, .T. ) ;
#6289=CARTESIAN_POINT ( 'NONE',  ( -1.279527559055117836, 1.968503937007873850, 2.480314960629921295 ) ) ;
#6296=PLANE ( 'NONE',  #6352 ) ;
#6343=ADVANCED_FACE ( 'NONE', ( #7360 ), #2133, .F. ) ;
#6352=AXIS2_PLACEMENT_3D ( 'NONE', #6866, #1621, #2808 ) ;
#6360=ADVANCED_FACE ( 'NONE', ( #6185, #2093, #1624 ), #3350, .F. ) ;
#6376=CIRCLE ( 'NONE', #6869, 0.2362204724409448231 ) ;
#6405=EDGE_CURVE ( 'NONE', #670, #4992, #1997, .T. ) ;
#6408=DIRECTION ( 'NONE',  ( -0.000000000000000000, -0.000000000000000000, -1.000000000000000000 ) ) ;
#6420=DIRECTION ( 'NONE',  ( 1.000000000000000000, 0.000000000000000000, 0.000000000000000000 ) ) ;
#6424=CARTESIAN_POINT ( 'NONE',  ( -2.834645669291338432, 0.000000000000000000, 0.000000000000000000 ) ) ;
#6425=FACE_OUTER_BOUND ( 'NONE', #463, .T. ) ;
#6427=ORIENTED_EDGE ( 'NONE', *, *, #1496, .F. ) ;
#6442=PLANE ( 'NONE',  #1718 ) ;
#6457=DIRECTION ( 'NONE',  ( -0.000000000000000000, -0.000000000000000000, 1.000000000000000000 ) ) ;
#6464=EDGE_LOOP ( 'NONE', ( #2669, #2991, #3344, #3640 ) ) ;
#6466=CARTESIAN_POINT ( 'NONE',  ( -0.7480314960629922405, 1.220472440944881942, 0.4724409448818898127 ) ) ;
#6499=FACE_OUTER_BOUND ( 'NONE', #4063, .T. ) ;
#6500=DIRECTION ( 'NONE',  ( -0.000000000000000000, -0.000000000000000000, -1.000000000000000000 ) ) ;
#6501=CARTESIAN_POINT ( 'NONE',  ( -0.7480314960629922405, 1.220472440944881942, 2.480314960629921295 ) ) ;
#6508=VERTEX_POINT ( 'NONE', #4036 ) ;
#6518=ORIENTED_EDGE ( 'NONE', *, *, #2480, .F. ) ;
#6532=DIRECTION ( 'NONE',  ( -0.000000000000000000, -0.000000000000000000, 1.000000000000000000 ) ) ;
#6542=CARTESIAN_POINT ( 'NONE',  ( 3.198568410424924124, 2.407012729153881203, 0.000000000000000000 ) ) ;
#6584=ORIENTED_EDGE ( 'NONE', *, *, #5010, .T. ) ;
#6585=AXIS2_PLACEMENT_3D ( 'NONE', #7174, #4847, #6614 ) ;
#6599=AXIS2_PLACEMENT_3D ( 'NONE', #2017, #6679, #3888 ) ;
#6614=DIRECTION ( 'NONE',  ( 1.000000000000000000, 0.000000000000000000, 0.000000000000000000 ) ) ;
#6632=VECTOR ( 'NONE', #342, 39.37007874015748143 ) ;
#6643=VECTOR ( 'NONE', #5122, 39.37007874015748143 ) ;
#6648=CARTESIAN_POINT ( 'NONE',  ( 0.7480314960629922405, 1.220472440944881942, 2.480314960629921295 ) ) ;
#6654=CARTESIAN_POINT ( 'NONE',  ( 0.7480314960629922405, 1.220472440944881942, 0.000000000000000000 ) ) ;
#6655=ORIENTED_EDGE ( 'NONE', *, *, #6224, .T. ) ;
#6678=EDGE_CURVE ( 'NONE', #7079, #670, #5108, .T. ) ;
#6679=DIRECTION ( 'NONE',  ( -0.000000000000000000, -0.000000000000000000, -1.000000000000000000 ) ) ;
#6690=EDGE_CURVE ( 'NONE', #1074, #6852, #1341, .T. ) ;
#6723=EDGE_LOOP ( 'NONE', ( #1707, #2088, #3697, #1642 ) ) ;
#6753=AXIS2_PLACEMENT_3D ( 'NONE', #6542, #2399, #5350 ) ;
#6755=DIRECTION ( 'NONE',  ( -1.000000000000000000, 0.000000000000000000, 0.000000000000000000 ) ) ;
#6774=DIRECTION ( 'NONE',  ( -0.000000000000000000, -0.000000000000000000, -1.000000000000000000 ) ) ;
#6776=ORIENTED_EDGE ( 'NONE', *, *, #6090, .F. ) ;
#6783=ORIENTED_EDGE ( 'NONE', *, *, #3656, .F. ) ;
#6796=CARTESIAN_POINT ( 'NONE',  ( 0.7480314960629922405, 1.220472440944881942, 2.480314960629921295 ) ) ;
#6797=( NAMED_UNIT ( * ) SI_UNIT ( $, .STERADIAN. ) SOLID_ANGLE_UNIT ( ) );
#6807=VERTEX_POINT ( 'NONE', #5313 ) ;
#6810=EDGE_LOOP ( 'NONE', ( #6655, #2930, #775, #7128, #5088, #7076 ) ) ;
#6815=ORIENTED_EDGE ( 'NONE', *, *, #5281, .T. ) ;
#6829=AXIS2_PLACEMENT_3D ( 'NONE', #6654, #7111, #1870 ) ;
#6831=LINE ( 'NONE', #2130, #5504 ) ;
#6837=EDGE_CURVE ( 'NONE', #6508, #4891, #7068, .T. ) ;
#6852=VERTEX_POINT ( 'NONE', #2927 ) ;
#6856=VERTEX_POINT ( 'NONE', #6012 ) ;
#6862=VERTEX_POINT ( 'NONE', #5237 ) ;
#6866=CARTESIAN_POINT ( 'NONE',  ( -2.834645669291338432, 0.000000000000000000, 0.4724409448818898127 ) ) ;
#6869=AXIS2_PLACEMENT_3D ( 'NONE', #4646, #4109, #3500 ) ;
#6878=EDGE_CURVE ( 'NONE', #7079, #7275, #988, .T. ) ;
#6879=DIRECTION ( 'NONE',  ( 0.000000000000000000, 0.000000000000000000, -1.000000000000000000 ) ) ;
#6885=CARTESIAN_POINT ( 'NONE',  ( 3.198568410424924124, 2.407012729153881203, 2.952755905511811108 ) ) ;
#6893=ORIENTED_EDGE ( 'NONE', *, *, #3645, .F. ) ;
#6899=ORIENTED_EDGE ( 'NONE', *, *, #2155, .F. ) ;
#6908=DIRECTION ( 'NONE',  ( -1.000000000000000000, 0.000000000000000000, 0.000000000000000000 ) ) ;
#6937=CARTESIAN_POINT ( 'NONE',  ( -0.5118110236220474452, 1.220472440944881942, 2.952755905511811108 ) ) ;
#6945=AXIS2_PLACEMENT_3D ( 'NONE', #3278, #5630, #3319 ) ;
#6956=PLANE ( 'NONE',  #5175 ) ;
#6968=CARTESIAN_POINT ( 'NONE',  ( -0.7480314960629922405, 1.220472440944881942, 2.480314960629921295 ) ) ;
#6971=CARTESIAN_POINT ( 'NONE',  ( 2.834645669291338432, 0.000000000000000000, 0.4724409448818898127 ) ) ;
#6978=CIRCLE ( 'NONE', #3688, 0.2362204724409448231 ) ;
#6983=DIRECTION ( 'NONE',  ( 1.000000000000000000, 0.000000000000000000, 0.000000000000000000 ) ) ;
#6991=DIRECTION ( 'NONE',  ( -0.000000000000000000, -0.000000000000000000, 1.000000000000000000 ) ) ;
#6992=EDGE_LOOP ( 'NONE', ( #4448, #6518 ) ) ;
#7010=ADVANCED_FACE ( 'NONE', ( #7016, #1768, #4108 ), #6442, .F. ) ;
#7016=FACE_BOUND ( 'NONE', #3450, .T. ) ;
#7017=LINE ( 'NONE', #3000, #1743 ) ;
#7022=PLANE ( 'NONE',  #1844 ) ;
#7030=DIRECTION ( 'NONE',  ( 1.000000000000000000, 0.000000000000000000, 0.000000000000000000 ) ) ;
#7043=CARTESIAN_POINT ( 'NONE',  ( -2.834645669291338432, 0.000000000000000000, 0.000000000000000000 ) ) ;
#7044=CIRCLE ( 'NONE', #5834, 0.2362204724409448231 ) ;
#7045=ORIENTED_EDGE ( 'NONE', *, *, #6690, .F. ) ;
#7048=ADVANCED_FACE ( 'NONE', ( #3174 ), #350, .F. ) ;
#7050=UNCERTAINTY_MEASURE_WITH_UNIT (LENGTH_MEASURE( 1.000000000000000082E-05 ), #6262, 'distance_accuracy_value', 'NONE');
#7054=DIRECTION ( 'NONE',  ( -1.000000000000000000, 0.000000000000000000, 0.000000000000000000 ) ) ;
#7068=LINE ( 'NONE', #1829, #4281 ) ;
#7072=FACE_OUTER_BOUND ( 'NONE', #7442, .T. ) ;
#7073=VECTOR ( 'NONE', #4957, 39.37007874015748143 ) ;
#7076=ORIENTED_EDGE ( 'NONE', *, *, #4581, .T. ) ;
#7079=VERTEX_POINT ( 'NONE', #4328 ) ;
#7094=VECTOR ( 'NONE', #832, 39.37007874015748143 ) ;
#7096=CARTESIAN_POINT ( 'NONE',  ( 1.279527559055118280, 1.968503937007874072, 0.000000000000000000 ) ) ;
#7107=AXIS2_PLACEMENT_3D ( 'NONE', #6971, #1082, #2804 ) ;
#7111=DIRECTION ( 'NONE',  ( 0.000000000000000000, 0.000000000000000000, 1.000000000000000000 ) ) ;
#7122=VECTOR ( 'NONE', #3039, 39.37007874015748143 ) ;
#7128=ORIENTED_EDGE ( 'NONE', *, *, #5197, .T. ) ;
#7151=EDGE_CURVE ( 'NONE', #3247, #428, #7210, .T. ) ;
#7174=CARTESIAN_POINT ( 'NONE',  ( 0.7480314960629922405, 1.220472440944881942, 0.4724409448818898127 ) ) ;
#7183=EDGE_CURVE ( 'NONE', #4943, #4985, #2818, .T. ) ;
#7202=CARTESIAN_POINT ( 'NONE',  ( -0.9842519685039370358, 1.220472440944881942, 2.480314960629921295 ) ) ;
#7208=FACE_OUTER_BOUND ( 'NONE', #5847, .T. ) ;
#7210=CIRCLE ( 'NONE', #4046, 0.2362204724409448231 ) ;
#7228=ORIENTED_EDGE ( 'NONE', *, *, #6126, .T. ) ;
#7230=EDGE_LOOP ( 'NONE', ( #4403, #1994, #6584, #5062 ) ) ;
#7253=CARTESIAN_POINT ( 'NONE',  ( -0.5118110236220474452, 1.220472440944881942, 0.4724409448818898127 ) ) ;
#7263=CARTESIAN_POINT ( 'NONE',  ( 2.834645669291338876, 0.4724409448818890911, 8.169257281319195485 ) ) ;
#7273=DIRECTION ( 'NONE',  ( 1.000000000000000000, 0.000000000000000000, 0.000000000000000000 ) ) ;
#7275=VERTEX_POINT ( 'NONE', #2964 ) ;
#7277=DIRECTION ( 'NONE',  ( -1.000000000000000000, 0.000000000000000000, 0.000000000000000000 ) ) ;
#7290=EDGE_LOOP ( 'NONE', ( #6199, #4087, #2040, #6899 ) ) ;
#7307=ORIENTED_EDGE ( 'NONE', *, *, #1343, .F. ) ;
#7352=ORIENTED_EDGE ( 'NONE', *, *, #664, .T. ) ;
#7360=FACE_OUTER_BOUND ( 'NONE', #7230, .T. ) ;
#7368=DIRECTION ( 'NONE',  ( -0.000000000000000000, -0.000000000000000000, -1.000000000000000000 ) ) ;
#7374=ADVANCED_FACE ( 'NONE', ( #1125 ), #7022, .F. ) ;
#7375=EDGE_CURVE ( 'NONE', #4992, #670, #6978, .T. ) ;
#7388=EDGE_LOOP ( 'NONE', ( #843, #3805, #2192, #7491 ) ) ;
#7425=ORIENTED_EDGE ( 'NONE', *, *, #6405, .T. ) ;
#7432=EDGE_CURVE ( 'NONE', #772, #6852, #909, .T. ) ;
#7434=DIRECTION ( 'NONE',  ( -0.000000000000000000, 0.000000000000000000, -1.000000000000000000 ) ) ;
#7439=FACE_OUTER_BOUND ( 'NONE', #3907, .T. ) ;
#7442=EDGE_LOOP ( 'NONE', ( #6281, #2149, #612, #2904 ) ) ;
#7456=ORIENTED_EDGE ( 'NONE', *, *, #7432, .F. ) ;
#7463=AXIS2_PLACEMENT_3D ( 'NONE', #3931, #7434, #3890 ) ;
#7470=ADVANCED_FACE ( 'NONE', ( #7208 ), #263, .F. ) ;
#7471=ADVANCED_FACE ( 'NONE', ( #6112 ), #2586, .F. ) ;
#7481=DIRECTION ( 'NONE',  ( 0.000000000000000000, -0.000000000000000000, 1.000000000000000000 ) ) ;
#7487=DIRECTION ( 'NONE',  ( 0.000000000000000000, -1.000000000000000000, 0.000000000000000000 ) ) ;
#7491=ORIENTED_EDGE ( 'NONE', *, *, #2066, .F. ) ;
#7496=ORIENTED_EDGE ( 'NONE', *, *, #2250, .T. ) ;
#7507=CARTESIAN_POINT ( 'NONE',  ( 0.5118110236220474452, 1.220472440944881942, 0.4724409448818898127 ) ) ;
#7553=COLOUR_RGB('Dark Blue',0.08,0.2,0.34);
#7554=FILL_AREA_STYLE_COLOUR('',#7553);
#7555=FILL_AREA_STYLE('',(#7554));
#7556=SURFACE_STYLE_FILL_AREA(#7555);
#7557=SURFACE_SIDE_STYLE('',(#7556));
#7558=SURFACE_STYLE_USAGE(.BOTH.,#7557);
#7559=PRESENTATION_STYLE_ASSIGNMENT((#7558));
ENDSEC;
END-ISO-10303-21;
